ISO-10303-21;
HEADER;
/* Generated by software containing ST-Developer
 * from STEP Tools, Inc. (www.steptools.com) 
 */

FILE_DESCRIPTION(
/* description */ ('STEP AP214'),
/* implementation_level */ '2;1');

FILE_NAME(
/* name */ 'Flat Washer M10 Narrow.step',
/* time_stamp */ '2026-11-14T06:43:04-08:00',
/* author */ (''),
/* organization */ (''),
/* preprocessor_version */ 'ST-DEVELOPER v20.2',
/* originating_system */ 'Autodesk Translation Framework v15.17.0.0',
/* authorisation */ '');

FILE_SCHEMA (('AUTOMOTIVE_DESIGN { 1 0 10303 214 3 1 1 }'));
ENDSEC;

DATA;
#10=MECHANICAL_DESIGN_GEOMETRIC_PRESENTATION_REPRESENTATION('',(#207),#5658);
#185=SHAPE_REPRESENTATION_RELATIONSHIP('SRR','None',#5715,#196);
#196=ADVANCED_BREP_SHAPE_REPRESENTATION('',(#218),#5656);
#207=STYLED_ITEM('',(#5770),#218);
#218=MANIFOLD_SOLID_BREP('Body1',#3069);
#267=CYLINDRICAL_SURFACE('',#3495,10.);
#268=CYLINDRICAL_SURFACE('',#3498,5.56);
#333=FACE_BOUND('',#741,.T.);
#334=FACE_BOUND('',#743,.T.);
#494=FACE_OUTER_BOUND('',#738,.T.);
#495=FACE_OUTER_BOUND('',#739,.T.);
#496=FACE_OUTER_BOUND('',#740,.T.);
#497=FACE_OUTER_BOUND('',#742,.T.);
#738=EDGE_LOOP('',(#2684,#2685,#2686,#2687));
#739=EDGE_LOOP('',(#2688,#2689,#2690,#2691));
#740=EDGE_LOOP('',(#2692));
#741=EDGE_LOOP('',(#2693));
#742=EDGE_LOOP('',(#2694));
#743=EDGE_LOOP('',(#2695));
#932=LINE('',#5510,#1128);
#933=LINE('',#5516,#1129);
#1128=VECTOR('',#4332,10.);
#1129=VECTOR('',#4339,5.56);
#1294=CIRCLE('',#3496,10.);
#1295=CIRCLE('',#3497,10.);
#1296=CIRCLE('',#3499,5.56);
#1297=CIRCLE('',#3500,5.56);
#1539=VERTEX_POINT('',#5507);
#1540=VERTEX_POINT('',#5509);
#1541=VERTEX_POINT('',#5513);
#1542=VERTEX_POINT('',#5515);
#1925=EDGE_CURVE('',#1539,#1539,#1294,.T.);
#1926=EDGE_CURVE('',#1539,#1540,#932,.T.);
#1927=EDGE_CURVE('',#1540,#1540,#1295,.T.);
#1928=EDGE_CURVE('',#1541,#1541,#1296,.T.);
#1929=EDGE_CURVE('',#1541,#1542,#933,.T.);
#1930=EDGE_CURVE('',#1542,#1542,#1297,.T.);
#2684=ORIENTED_EDGE('',*,*,#1925,.F.);
#2685=ORIENTED_EDGE('',*,*,#1926,.T.);
#2686=ORIENTED_EDGE('',*,*,#1927,.T.);
#2687=ORIENTED_EDGE('',*,*,#1926,.F.);
#2688=ORIENTED_EDGE('',*,*,#1928,.F.);
#2689=ORIENTED_EDGE('',*,*,#1929,.T.);
#2690=ORIENTED_EDGE('',*,*,#1930,.T.);
#2691=ORIENTED_EDGE('',*,*,#1929,.F.);
#2692=ORIENTED_EDGE('',*,*,#1927,.F.);
#2693=ORIENTED_EDGE('',*,*,#1928,.T.);
#2694=ORIENTED_EDGE('',*,*,#1925,.T.);
#2695=ORIENTED_EDGE('',*,*,#1930,.F.);
#2861=PLANE('',#3501);
#2862=PLANE('',#3502);
#3035=ADVANCED_FACE('',(#494),#267,.T.);
#3036=ADVANCED_FACE('',(#495),#268,.F.);
#3037=ADVANCED_FACE('',(#496,#333),#2861,.F.);
#3038=ADVANCED_FACE('',(#497,#334),#2862,.F.);
#3069=CLOSED_SHELL('',(#3035,#3036,#3037,#3038));
#3494=AXIS2_PLACEMENT_3D('',#5505,#4326,#4327);
#3495=AXIS2_PLACEMENT_3D('',#5506,#4328,#4329);
#3496=AXIS2_PLACEMENT_3D('',#5508,#4330,#4331);
#3497=AXIS2_PLACEMENT_3D('',#5511,#4333,#4334);
#3498=AXIS2_PLACEMENT_3D('',#5512,#4335,#4336);
#3499=AXIS2_PLACEMENT_3D('',#5514,#4337,#4338);
#3500=AXIS2_PLACEMENT_3D('',#5517,#4340,#4341);
#3501=AXIS2_PLACEMENT_3D('',#5518,#4342,#4343);
#3502=AXIS2_PLACEMENT_3D('',#5519,#4344,#4345);
#4326=DIRECTION('axis',(0.,0.,1.));
#4327=DIRECTION('refdir',(1.,0.,0.));
#4328=DIRECTION('center_axis',(-1.,0.,0.));
#4329=DIRECTION('ref_axis',(0.,0.,1.));
#4330=DIRECTION('center_axis',(-1.,0.,0.));
#4331=DIRECTION('ref_axis',(0.,0.,1.));
#4332=DIRECTION('',(1.,0.,0.));
#4333=DIRECTION('center_axis',(-1.,0.,0.));
#4334=DIRECTION('ref_axis',(0.,0.,1.));
#4335=DIRECTION('center_axis',(-1.,0.,0.));
#4336=DIRECTION('ref_axis',(0.,0.,1.));
#4337=DIRECTION('center_axis',(-1.,0.,0.));
#4338=DIRECTION('ref_axis',(0.,0.,1.));
#4339=DIRECTION('',(-1.,0.,0.));
#4340=DIRECTION('center_axis',(-1.,0.,0.));
#4341=DIRECTION('ref_axis',(0.,0.,1.));
#4342=DIRECTION('center_axis',(-1.,0.,0.));
#4343=DIRECTION('ref_axis',(0.,0.,1.));
#4344=DIRECTION('center_axis',(1.,0.,0.));
#4345=DIRECTION('ref_axis',(0.,0.,-1.));
#5505=CARTESIAN_POINT('',(0.,0.,0.));
#5506=CARTESIAN_POINT('Origin',(-34.9249999999999,0.,0.));
#5507=CARTESIAN_POINT('',(-2.3,-1.22464679914735E-15,-10.));
#5508=CARTESIAN_POINT('Origin',(-2.3,0.,0.));
#5509=CARTESIAN_POINT('',(0.,-1.22464679914735E-15,-10.));
#5510=CARTESIAN_POINT('',(-34.9249999999999,-1.22464679914735E-15,-10.));
#5511=CARTESIAN_POINT('Origin',(0.,0.,0.));
#5512=CARTESIAN_POINT('Origin',(-34.9249999999999,0.,0.));
#5513=CARTESIAN_POINT('',(0.,-6.80903620325928E-16,-5.56));
#5514=CARTESIAN_POINT('Origin',(0.,0.,0.));
#5515=CARTESIAN_POINT('',(-2.3,-6.80903620325928E-16,-5.56));
#5516=CARTESIAN_POINT('',(-34.9249999999999,-6.80903620325928E-16,-5.56));
#5517=CARTESIAN_POINT('Origin',(-2.3,0.,0.));
#5518=CARTESIAN_POINT('Origin',(0.,5.56,0.));
#5519=CARTESIAN_POINT('Origin',(-2.3,10.,0.));
#5643=UNCERTAINTY_MEASURE_WITH_UNIT(LENGTH_MEASURE(0.01),#5659,
'DISTANCE_ACCURACY_VALUE',
'Maximum model space distance between geometric entities at asserted c
onnectivities');
#5645=UNCERTAINTY_MEASURE_WITH_UNIT(LENGTH_MEASURE(0.01),#5659,
'DISTANCE_ACCURACY_VALUE',
'Maximum model space distance between geometric entities at asserted c
onnectivities');
#5656=(
GEOMETRIC_REPRESENTATION_CONTEXT(3)
GLOBAL_UNCERTAINTY_ASSIGNED_CONTEXT((#5643))
GLOBAL_UNIT_ASSIGNED_CONTEXT((#5659,#5661,#5662))
REPRESENTATION_CONTEXT('','3D')
);
#5658=(
GEOMETRIC_REPRESENTATION_CONTEXT(3)
GLOBAL_UNCERTAINTY_ASSIGNED_CONTEXT((#5645))
GLOBAL_UNIT_ASSIGNED_CONTEXT((#5659,#5661,#5662))
REPRESENTATION_CONTEXT('','3D')
);
#5659=(
LENGTH_UNIT()
NAMED_UNIT(*)
SI_UNIT(.MILLI.,.METRE.)
);
#5661=(
NAMED_UNIT(*)
PLANE_ANGLE_UNIT()
SI_UNIT($,.RADIAN.)
);
#5662=(
NAMED_UNIT(*)
SI_UNIT($,.STERADIAN.)
SOLID_ANGLE_UNIT()
);
#5673=SHAPE_DEFINITION_REPRESENTATION(#5685,#5715);
#5685=PRODUCT_DEFINITION_SHAPE('',$,#5728);
#5715=SHAPE_REPRESENTATION('',(#3494),#5656);
#5717=PRODUCT_DEFINITION_CONTEXT('part definition',#5755,'design');
#5728=PRODUCT_DEFINITION('Flat Washer M10 Narrow',
'Flat Washer M10 Narrow',#5740,#5717);
#5740=PRODUCT_DEFINITION_FORMATION('',$,#5767);
#5755=APPLICATION_CONTEXT(
'Core Data for Automotive Mechanical Design Process');
#5756=PRODUCT_CONTEXT('part definition',#5755,'mechanical');
#5767=PRODUCT('Flat Washer M10 Narrow','Flat Washer M10 Narrow',$,(#5756));
#5770=PRESENTATION_STYLE_ASSIGNMENT((#5775));
#5775=SURFACE_STYLE_USAGE(.BOTH.,#5780);
#5780=SURFACE_SIDE_STYLE('',(#5785));
#5785=SURFACE_STYLE_FILL_AREA(#5790);
#5790=FILL_AREA_STYLE('Opaque(31,36,43)',(#5795));
#5795=FILL_AREA_STYLE_COLOUR('Opaque(31,36,43)',#5800);
#5800=COLOUR_RGB('Opaque(31,36,43)',0.12156862745098,0.141176470588235,
0.168627450980392);
ENDSEC;
END-ISO-10303-21;
